ISO-10303-21;
HEADER;
/* Generated by software containing ST-Developer
 * from STEP Tools, Inc. (www.steptools.com) 
 */

FILE_DESCRIPTION(
/* description */ ('PAT-096'),
/* implementation_level */ '2;1');

FILE_NAME(
/* name */ 'M5x14 Cap Screw.step',
/* time_stamp */ '2026-10-29T17:03:14-07:00',
/* author */ (''),
/* organization */ (''),
/* preprocessor_version */ 'ST-DEVELOPER v20.2',
/* originating_system */ 'Autodesk Translation Framework v15.17.0.0',
/* authorisation */ '');

FILE_SCHEMA (('AUTOMOTIVE_DESIGN { 1 0 10303 214 3 1 1 }'));
ENDSEC;

DATA;
#10=MECHANICAL_DESIGN_GEOMETRIC_PRESENTATION_REPRESENTATION('',(#399),#10650);
#312=CONICAL_SURFACE('',#5961,0.4,0.785398163397448);
#313=CONICAL_SURFACE('',#5965,0.41,0.785398163397448);
#314=CONICAL_SURFACE('',#5969,0.26,0.463647609000806);
#330=ORIENTED_CLOSED_SHELL('',*,#5532,.F.);
#333=BREP_WITH_VOIDS('Body1',#5533,(#330));
#337=SHAPE_REPRESENTATION_RELATIONSHIP('SRR','None',#10797,#368);
#368=ADVANCED_BREP_SHAPE_REPRESENTATION('',(#333),#10615);
#399=STYLED_ITEM('',(#11071),#333);
#489=FACE_BOUND('',#1170,.T.);
#618=PLANE('',#5949);
#619=PLANE('',#5950);
#620=PLANE('',#5951);
#621=PLANE('',#5952);
#622=PLANE('',#5953);
#623=PLANE('',#5954);
#624=PLANE('',#5955);
#625=PLANE('',#5956);
#626=PLANE('',#5957);
#627=PLANE('',#5959);
#628=PLANE('',#5967);
#804=FACE_OUTER_BOUND('',#1156,.T.);
#805=FACE_OUTER_BOUND('',#1157,.T.);
#806=FACE_OUTER_BOUND('',#1158,.T.);
#807=FACE_OUTER_BOUND('',#1159,.T.);
#808=FACE_OUTER_BOUND('',#1160,.T.);
#809=FACE_OUTER_BOUND('',#1161,.T.);
#810=FACE_OUTER_BOUND('',#1162,.T.);
#811=FACE_OUTER_BOUND('',#1163,.T.);
#812=FACE_OUTER_BOUND('',#1164,.T.);
#813=FACE_OUTER_BOUND('',#1165,.T.);
#814=FACE_OUTER_BOUND('',#1166,.T.);
#815=FACE_OUTER_BOUND('',#1167,.T.);
#816=FACE_OUTER_BOUND('',#1168,.T.);
#817=FACE_OUTER_BOUND('',#1169,.T.);
#818=FACE_OUTER_BOUND('',#1171,.T.);
#819=FACE_OUTER_BOUND('',#1172,.T.);
#1156=EDGE_LOOP('',(#3787,#3788,#3789,#3790));
#1157=EDGE_LOOP('',(#3791,#3792,#3793,#3794));
#1158=EDGE_LOOP('',(#3795,#3796,#3797,#3798));
#1159=EDGE_LOOP('',(#3799,#3800,#3801,#3802));
#1160=EDGE_LOOP('',(#3803,#3804,#3805,#3806));
#1161=EDGE_LOOP('',(#3807,#3808,#3809,#3810));
#1162=EDGE_LOOP('',(#3811,#3812,#3813,#3814,#3815,#3816));
#1163=EDGE_LOOP('',(#3817,#3818,#3819,#3820,#3821,#3822));
#1164=EDGE_LOOP('',(#3823));
#1165=EDGE_LOOP('',(#3824));
#1166=EDGE_LOOP('',(#3825,#3826,#3827,#3828));
#1167=EDGE_LOOP('',(#3829,#3830,#3831,#3832));
#1168=EDGE_LOOP('',(#3833,#3834,#3835,#3836));
#1169=EDGE_LOOP('',(#3837));
#1170=EDGE_LOOP('',(#3838));
#1171=EDGE_LOOP('',(#3839,#3840,#3841,#3842));
#1172=EDGE_LOOP('',(#3843,#3844,#3845,#3846));
#1621=LINE('',#8593,#1950);
#1622=LINE('',#8595,#1951);
#1623=LINE('',#8597,#1952);
#1624=LINE('',#8598,#1953);
#1625=LINE('',#8601,#1954);
#1626=LINE('',#8603,#1955);
#1627=LINE('',#8604,#1956);
#1628=LINE('',#8607,#1957);
#1629=LINE('',#8609,#1958);
#1630=LINE('',#8610,#1959);
#1631=LINE('',#8613,#1960);
#1632=LINE('',#8615,#1961);
#1633=LINE('',#8616,#1962);
#1634=LINE('',#8619,#1963);
#1635=LINE('',#8621,#1964);
#1636=LINE('',#8622,#1965);
#1637=LINE('',#8624,#1966);
#1638=LINE('',#8625,#1967);
#1639=LINE('',#8637,#1968);
#1640=LINE('',#8641,#1969);
#1641=LINE('',#8645,#1970);
#1642=LINE('',#8652,#1971);
#1643=LINE('',#8654,#1972);
#1950=VECTOR('',#6761,1.);
#1951=VECTOR('',#6762,1.);
#1952=VECTOR('',#6763,1.);
#1953=VECTOR('',#6764,1.);
#1954=VECTOR('',#6767,1.);
#1955=VECTOR('',#6768,1.);
#1956=VECTOR('',#6769,1.);
#1957=VECTOR('',#6772,1.);
#1958=VECTOR('',#6773,1.);
#1959=VECTOR('',#6774,1.);
#1960=VECTOR('',#6777,1.);
#1961=VECTOR('',#6778,1.);
#1962=VECTOR('',#6779,1.);
#1963=VECTOR('',#6782,1.);
#1964=VECTOR('',#6783,1.);
#1965=VECTOR('',#6784,1.);
#1966=VECTOR('',#6787,1.);
#1967=VECTOR('',#6788,1.);
#1968=VECTOR('',#6805,0.4);
#1969=VECTOR('',#6810,0.425);
#1970=VECTOR('',#6815,0.41);
#1971=VECTOR('',#6824,0.26);
#1972=VECTOR('',#6827,0.25);
#2275=CIRCLE('',#5958,0.24505);
#2276=CIRCLE('',#5960,0.375);
#2277=CIRCLE('',#5962,0.425);
#2278=CIRCLE('',#5964,0.425);
#2279=CIRCLE('',#5966,0.395);
#2280=CIRCLE('',#5968,0.27);
#2281=CIRCLE('',#5970,0.24505);
#2602=VERTEX_POINT('',#8591);
#2603=VERTEX_POINT('',#8592);
#2604=VERTEX_POINT('',#8594);
#2605=VERTEX_POINT('',#8596);
#2606=VERTEX_POINT('',#8600);
#2607=VERTEX_POINT('',#8602);
#2608=VERTEX_POINT('',#8606);
#2609=VERTEX_POINT('',#8608);
#2610=VERTEX_POINT('',#8612);
#2611=VERTEX_POINT('',#8614);
#2612=VERTEX_POINT('',#8618);
#2613=VERTEX_POINT('',#8620);
#2614=VERTEX_POINT('',#8629);
#2615=VERTEX_POINT('',#8632);
#2616=VERTEX_POINT('',#8635);
#2617=VERTEX_POINT('',#8639);
#2618=VERTEX_POINT('',#8643);
#2619=VERTEX_POINT('',#8647);
#2620=VERTEX_POINT('',#8650);
#3072=EDGE_CURVE('',#2602,#2603,#1621,.T.);
#3073=EDGE_CURVE('',#2603,#2604,#1622,.T.);
#3074=EDGE_CURVE('',#2604,#2605,#1623,.T.);
#3075=EDGE_CURVE('',#2602,#2605,#1624,.T.);
#3076=EDGE_CURVE('',#2603,#2606,#1625,.T.);
#3077=EDGE_CURVE('',#2606,#2607,#1626,.T.);
#3078=EDGE_CURVE('',#2607,#2604,#1627,.T.);
#3079=EDGE_CURVE('',#2606,#2608,#1628,.T.);
#3080=EDGE_CURVE('',#2608,#2609,#1629,.T.);
#3081=EDGE_CURVE('',#2609,#2607,#1630,.T.);
#3082=EDGE_CURVE('',#2608,#2610,#1631,.T.);
#3083=EDGE_CURVE('',#2610,#2611,#1632,.T.);
#3084=EDGE_CURVE('',#2611,#2609,#1633,.T.);
#3085=EDGE_CURVE('',#2610,#2612,#1634,.T.);
#3086=EDGE_CURVE('',#2612,#2613,#1635,.T.);
#3087=EDGE_CURVE('',#2613,#2611,#1636,.T.);
#3088=EDGE_CURVE('',#2612,#2602,#1637,.T.);
#3089=EDGE_CURVE('',#2605,#2613,#1638,.T.);
#3090=EDGE_CURVE('',#2614,#2614,#2275,.T.);
#3091=EDGE_CURVE('',#2615,#2615,#2276,.T.);
#3092=EDGE_CURVE('',#2616,#2616,#2277,.T.);
#3093=EDGE_CURVE('',#2616,#2615,#1639,.T.);
#3094=EDGE_CURVE('',#2617,#2617,#2278,.T.);
#3095=EDGE_CURVE('',#2617,#2616,#1640,.T.);
#3096=EDGE_CURVE('',#2618,#2618,#2279,.T.);
#3097=EDGE_CURVE('',#2618,#2617,#1641,.T.);
#3098=EDGE_CURVE('',#2619,#2619,#2280,.T.);
#3099=EDGE_CURVE('',#2620,#2620,#2281,.F.);
#3100=EDGE_CURVE('',#2620,#2619,#1642,.T.);
#3101=EDGE_CURVE('',#2614,#2620,#1643,.T.);
#3787=ORIENTED_EDGE('',*,*,#3072,.T.);
#3788=ORIENTED_EDGE('',*,*,#3073,.T.);
#3789=ORIENTED_EDGE('',*,*,#3074,.T.);
#3790=ORIENTED_EDGE('',*,*,#3075,.F.);
#3791=ORIENTED_EDGE('',*,*,#3076,.T.);
#3792=ORIENTED_EDGE('',*,*,#3077,.T.);
#3793=ORIENTED_EDGE('',*,*,#3078,.T.);
#3794=ORIENTED_EDGE('',*,*,#3073,.F.);
#3795=ORIENTED_EDGE('',*,*,#3079,.T.);
#3796=ORIENTED_EDGE('',*,*,#3080,.T.);
#3797=ORIENTED_EDGE('',*,*,#3081,.T.);
#3798=ORIENTED_EDGE('',*,*,#3077,.F.);
#3799=ORIENTED_EDGE('',*,*,#3082,.T.);
#3800=ORIENTED_EDGE('',*,*,#3083,.T.);
#3801=ORIENTED_EDGE('',*,*,#3084,.T.);
#3802=ORIENTED_EDGE('',*,*,#3080,.F.);
#3803=ORIENTED_EDGE('',*,*,#3085,.T.);
#3804=ORIENTED_EDGE('',*,*,#3086,.T.);
#3805=ORIENTED_EDGE('',*,*,#3087,.T.);
#3806=ORIENTED_EDGE('',*,*,#3083,.F.);
#3807=ORIENTED_EDGE('',*,*,#3088,.T.);
#3808=ORIENTED_EDGE('',*,*,#3075,.T.);
#3809=ORIENTED_EDGE('',*,*,#3089,.T.);
#3810=ORIENTED_EDGE('',*,*,#3086,.F.);
#3811=ORIENTED_EDGE('',*,*,#3088,.F.);
#3812=ORIENTED_EDGE('',*,*,#3085,.F.);
#3813=ORIENTED_EDGE('',*,*,#3082,.F.);
#3814=ORIENTED_EDGE('',*,*,#3079,.F.);
#3815=ORIENTED_EDGE('',*,*,#3076,.F.);
#3816=ORIENTED_EDGE('',*,*,#3072,.F.);
#3817=ORIENTED_EDGE('',*,*,#3089,.F.);
#3818=ORIENTED_EDGE('',*,*,#3074,.F.);
#3819=ORIENTED_EDGE('',*,*,#3078,.F.);
#3820=ORIENTED_EDGE('',*,*,#3081,.F.);
#3821=ORIENTED_EDGE('',*,*,#3084,.F.);
#3822=ORIENTED_EDGE('',*,*,#3087,.F.);
#3823=ORIENTED_EDGE('',*,*,#3090,.F.);
#3824=ORIENTED_EDGE('',*,*,#3091,.F.);
#3825=ORIENTED_EDGE('',*,*,#3092,.F.);
#3826=ORIENTED_EDGE('',*,*,#3093,.T.);
#3827=ORIENTED_EDGE('',*,*,#3091,.T.);
#3828=ORIENTED_EDGE('',*,*,#3093,.F.);
#3829=ORIENTED_EDGE('',*,*,#3094,.F.);
#3830=ORIENTED_EDGE('',*,*,#3095,.T.);
#3831=ORIENTED_EDGE('',*,*,#3092,.T.);
#3832=ORIENTED_EDGE('',*,*,#3095,.F.);
#3833=ORIENTED_EDGE('',*,*,#3096,.F.);
#3834=ORIENTED_EDGE('',*,*,#3097,.T.);
#3835=ORIENTED_EDGE('',*,*,#3094,.T.);
#3836=ORIENTED_EDGE('',*,*,#3097,.F.);
#3837=ORIENTED_EDGE('',*,*,#3096,.T.);
#3838=ORIENTED_EDGE('',*,*,#3098,.F.);
#3839=ORIENTED_EDGE('',*,*,#3099,.F.);
#3840=ORIENTED_EDGE('',*,*,#3100,.T.);
#3841=ORIENTED_EDGE('',*,*,#3098,.T.);
#3842=ORIENTED_EDGE('',*,*,#3100,.F.);
#3843=ORIENTED_EDGE('',*,*,#3090,.T.);
#3844=ORIENTED_EDGE('',*,*,#3101,.T.);
#3845=ORIENTED_EDGE('',*,*,#3099,.T.);
#3846=ORIENTED_EDGE('',*,*,#3101,.F.);
#5081=CYLINDRICAL_SURFACE('',#5963,0.425);
#5082=CYLINDRICAL_SURFACE('',#5971,0.24505);
#5209=ADVANCED_FACE('',(#804),#618,.F.);
#5210=ADVANCED_FACE('',(#805),#619,.F.);
#5211=ADVANCED_FACE('',(#806),#620,.F.);
#5212=ADVANCED_FACE('',(#807),#621,.F.);
#5213=ADVANCED_FACE('',(#808),#622,.F.);
#5214=ADVANCED_FACE('',(#809),#623,.F.);
#5215=ADVANCED_FACE('',(#810),#624,.F.);
#5216=ADVANCED_FACE('',(#811),#625,.F.);
#5217=ADVANCED_FACE('',(#812),#626,.F.);
#5218=ADVANCED_FACE('',(#813),#627,.T.);
#5219=ADVANCED_FACE('',(#814),#312,.T.);
#5220=ADVANCED_FACE('',(#815),#5081,.T.);
#5221=ADVANCED_FACE('',(#816),#313,.T.);
#5222=ADVANCED_FACE('',(#817,#489),#628,.T.);
#5223=ADVANCED_FACE('',(#818),#314,.T.);
#5224=ADVANCED_FACE('',(#819),#5082,.T.);
#5532=CLOSED_SHELL('',(#5209,#5210,#5211,#5212,#5213,#5214,#5215,#5216));
#5533=CLOSED_SHELL('',(#5217,#5218,#5219,#5220,#5221,#5222,#5223,#5224));
#5948=AXIS2_PLACEMENT_3D('',#8589,#6757,#6758);
#5949=AXIS2_PLACEMENT_3D('',#8590,#6759,#6760);
#5950=AXIS2_PLACEMENT_3D('',#8599,#6765,#6766);
#5951=AXIS2_PLACEMENT_3D('',#8605,#6770,#6771);
#5952=AXIS2_PLACEMENT_3D('',#8611,#6775,#6776);
#5953=AXIS2_PLACEMENT_3D('',#8617,#6780,#6781);
#5954=AXIS2_PLACEMENT_3D('',#8623,#6785,#6786);
#5955=AXIS2_PLACEMENT_3D('',#8626,#6789,#6790);
#5956=AXIS2_PLACEMENT_3D('',#8627,#6791,#6792);
#5957=AXIS2_PLACEMENT_3D('',#8628,#6793,#6794);
#5958=AXIS2_PLACEMENT_3D('',#8630,#6795,#6796);
#5959=AXIS2_PLACEMENT_3D('',#8631,#6797,#6798);
#5960=AXIS2_PLACEMENT_3D('',#8633,#6799,#6800);
#5961=AXIS2_PLACEMENT_3D('',#8634,#6801,#6802);
#5962=AXIS2_PLACEMENT_3D('',#8636,#6803,#6804);
#5963=AXIS2_PLACEMENT_3D('',#8638,#6806,#6807);
#5964=AXIS2_PLACEMENT_3D('',#8640,#6808,#6809);
#5965=AXIS2_PLACEMENT_3D('',#8642,#6811,#6812);
#5966=AXIS2_PLACEMENT_3D('',#8644,#6813,#6814);
#5967=AXIS2_PLACEMENT_3D('',#8646,#6816,#6817);
#5968=AXIS2_PLACEMENT_3D('',#8648,#6818,#6819);
#5969=AXIS2_PLACEMENT_3D('',#8649,#6820,#6821);
#5970=AXIS2_PLACEMENT_3D('',#8651,#6822,#6823);
#5971=AXIS2_PLACEMENT_3D('',#8653,#6825,#6826);
#6757=DIRECTION('axis',(0.,0.,1.));
#6758=DIRECTION('refdir',(1.,0.,0.));
#6759=DIRECTION('center_axis',(0.866025403784439,0.,-0.5));
#6760=DIRECTION('ref_axis',(0.5,0.,0.866025403784439));
#6761=DIRECTION('',(-0.5,0.,-0.866025403784439));
#6762=DIRECTION('',(0.,-1.,0.));
#6763=DIRECTION('',(0.5,0.,0.866025403784439));
#6764=DIRECTION('',(0.,-1.,0.));
#6765=DIRECTION('center_axis',(1.20185167898973E-16,0.,-1.));
#6766=DIRECTION('ref_axis',(1.,0.,1.20185167898973E-16));
#6767=DIRECTION('',(-1.,0.,-1.20185167898973E-16));
#6768=DIRECTION('',(0.,-1.,0.));
#6769=DIRECTION('',(1.,0.,1.20185167898973E-16));
#6770=DIRECTION('center_axis',(-0.866025403784439,0.,-0.5));
#6771=DIRECTION('ref_axis',(0.5,0.,-0.866025403784439));
#6772=DIRECTION('',(-0.5,0.,0.866025403784439));
#6773=DIRECTION('',(0.,-1.,0.));
#6774=DIRECTION('',(0.5,0.,-0.866025403784439));
#6775=DIRECTION('center_axis',(-0.866025403784439,0.,0.5));
#6776=DIRECTION('ref_axis',(-0.5,0.,-0.866025403784439));
#6777=DIRECTION('',(0.5,0.,0.866025403784439));
#6778=DIRECTION('',(0.,-1.,0.));
#6779=DIRECTION('',(-0.5,0.,-0.866025403784439));
#6780=DIRECTION('center_axis',(-2.40370335797945E-16,0.,1.));
#6781=DIRECTION('ref_axis',(-1.,0.,-2.40370335797945E-16));
#6782=DIRECTION('',(1.,0.,2.40370335797945E-16));
#6783=DIRECTION('',(0.,-1.,0.));
#6784=DIRECTION('',(-1.,0.,-2.40370335797945E-16));
#6785=DIRECTION('center_axis',(0.866025403784439,0.,0.5));
#6786=DIRECTION('ref_axis',(-0.5,0.,0.866025403784439));
#6787=DIRECTION('',(0.5,0.,-0.866025403784439));
#6788=DIRECTION('',(-0.5,0.,0.866025403784439));
#6789=DIRECTION('center_axis',(0.,1.,0.));
#6790=DIRECTION('ref_axis',(1.,0.,0.));
#6791=DIRECTION('center_axis',(0.,-1.,0.));
#6792=DIRECTION('ref_axis',(0.,0.,-1.));
#6793=DIRECTION('center_axis',(0.,1.,0.));
#6794=DIRECTION('ref_axis',(1.,0.,0.));
#6795=DIRECTION('center_axis',(0.,1.,0.));
#6796=DIRECTION('ref_axis',(1.,0.,0.));
#6797=DIRECTION('center_axis',(0.,1.,0.));
#6798=DIRECTION('ref_axis',(0.,0.,1.));
#6799=DIRECTION('center_axis',(0.,-1.,0.));
#6800=DIRECTION('ref_axis',(1.,0.,0.));
#6801=DIRECTION('center_axis',(0.,-1.,0.));
#6802=DIRECTION('ref_axis',(1.,0.,0.));
#6803=DIRECTION('center_axis',(0.,-1.,0.));
#6804=DIRECTION('ref_axis',(1.,0.,0.));
#6805=DIRECTION('',(0.707106781186548,0.707106781186547,8.65956056235493E-17));
#6806=DIRECTION('center_axis',(0.,-1.,0.));
#6807=DIRECTION('ref_axis',(1.,0.,0.));
#6808=DIRECTION('center_axis',(0.,-1.,0.));
#6809=DIRECTION('ref_axis',(1.,0.,0.));
#6810=DIRECTION('',(0.,1.,0.));
#6811=DIRECTION('center_axis',(0.,1.,0.));
#6812=DIRECTION('ref_axis',(1.,0.,0.));
#6813=DIRECTION('center_axis',(0.,-1.,0.));
#6814=DIRECTION('ref_axis',(1.,0.,0.));
#6815=DIRECTION('',(-0.707106781186547,0.707106781186548,-8.65956056235493E-17));
#6816=DIRECTION('center_axis',(0.,-1.,0.));
#6817=DIRECTION('ref_axis',(0.,0.,-1.));
#6818=DIRECTION('center_axis',(0.,-1.,0.));
#6819=DIRECTION('ref_axis',(1.,0.,0.));
#6820=DIRECTION('center_axis',(0.,1.,0.));
#6821=DIRECTION('ref_axis',(1.,0.,0.));
#6822=DIRECTION('center_axis',(0.,1.,0.));
#6823=DIRECTION('ref_axis',(1.,0.,0.));
#6824=DIRECTION('',(-0.447213595499958,0.894427190999916,-5.47678698264203E-17));
#6825=DIRECTION('center_axis',(0.,-1.,0.));
#6826=DIRECTION('ref_axis',(1.,0.,0.));
#6827=DIRECTION('',(0.,1.,0.));
#8589=CARTESIAN_POINT('',(0.,0.,0.));
#8590=CARTESIAN_POINT('Origin',(0.115470053837925,-0.5,-0.2));
#8591=CARTESIAN_POINT('',(0.23094010767585,-0.5,0.));
#8592=CARTESIAN_POINT('',(0.115470053837925,-0.5,-0.2));
#8593=CARTESIAN_POINT('',(0.23094010767585,-0.5,0.));
#8594=CARTESIAN_POINT('',(0.115470053837925,-0.8,-0.2));
#8595=CARTESIAN_POINT('',(0.115470053837925,-0.5,-0.2));
#8596=CARTESIAN_POINT('',(0.23094010767585,-0.8,0.));
#8597=CARTESIAN_POINT('',(0.23094010767585,-0.8,0.));
#8598=CARTESIAN_POINT('',(0.23094010767585,-0.5,0.));
#8599=CARTESIAN_POINT('Origin',(-0.115470053837925,-0.5,-0.2));
#8600=CARTESIAN_POINT('',(-0.115470053837925,-0.5,-0.2));
#8601=CARTESIAN_POINT('',(0.115470053837925,-0.5,-0.2));
#8602=CARTESIAN_POINT('',(-0.115470053837925,-0.8,-0.2));
#8603=CARTESIAN_POINT('',(-0.115470053837925,-0.5,-0.2));
#8604=CARTESIAN_POINT('',(0.115470053837925,-0.8,-0.2));
#8605=CARTESIAN_POINT('Origin',(-0.23094010767585,-0.5,-2.77555756156289E-17));
#8606=CARTESIAN_POINT('',(-0.23094010767585,-0.5,-2.82820063659975E-17));
#8607=CARTESIAN_POINT('',(-0.115470053837925,-0.5,-0.2));
#8608=CARTESIAN_POINT('',(-0.23094010767585,-0.8,-2.77555756156289E-17));
#8609=CARTESIAN_POINT('',(-0.23094010767585,-0.5,-2.82820063659975E-17));
#8610=CARTESIAN_POINT('',(-0.115470053837925,-0.8,-0.2));
#8611=CARTESIAN_POINT('Origin',(-0.115470053837925,-0.5,0.2));
#8612=CARTESIAN_POINT('',(-0.115470053837925,-0.5,0.2));
#8613=CARTESIAN_POINT('',(-0.23094010767585,-0.5,-2.82820063659975E-17));
#8614=CARTESIAN_POINT('',(-0.115470053837925,-0.8,0.2));
#8615=CARTESIAN_POINT('',(-0.115470053837925,-0.5,0.2));
#8616=CARTESIAN_POINT('',(-0.23094010767585,-0.8,-2.82820063659975E-17));
#8617=CARTESIAN_POINT('Origin',(0.115470053837925,-0.5,0.2));
#8618=CARTESIAN_POINT('',(0.115470053837925,-0.5,0.2));
#8619=CARTESIAN_POINT('',(-0.115470053837925,-0.5,0.2));
#8620=CARTESIAN_POINT('',(0.115470053837925,-0.8,0.2));
#8621=CARTESIAN_POINT('',(0.115470053837925,-0.5,0.2));
#8622=CARTESIAN_POINT('',(-0.115470053837925,-0.8,0.2));
#8623=CARTESIAN_POINT('Origin',(0.23094010767585,-0.5,0.));
#8624=CARTESIAN_POINT('',(0.115470053837925,-0.5,0.2));
#8625=CARTESIAN_POINT('',(0.115470053837925,-0.8,0.2));
#8626=CARTESIAN_POINT('Origin',(0.,-0.5,0.));
#8627=CARTESIAN_POINT('Origin',(0.,-0.8,0.));
#8628=CARTESIAN_POINT('Origin',(0.,-1.4,0.));
#8629=CARTESIAN_POINT('',(-0.24505,-1.4,3.00099698131059E-17));
#8630=CARTESIAN_POINT('Origin',(0.,-1.4,0.));
#8631=CARTESIAN_POINT('Origin',(0.375,0.5,0.));
#8632=CARTESIAN_POINT('',(-0.375,0.5,-4.59242549680257E-17));
#8633=CARTESIAN_POINT('Origin',(0.,0.5,0.));
#8634=CARTESIAN_POINT('Origin',(0.,0.475,0.));
#8635=CARTESIAN_POINT('',(-0.425,0.45,-5.20474889637625E-17));
#8636=CARTESIAN_POINT('Origin',(0.,0.45,0.));
#8637=CARTESIAN_POINT('',(-0.4,0.475,-4.89858719658941E-17));
#8638=CARTESIAN_POINT('Origin',(0.,0.24,0.));
#8639=CARTESIAN_POINT('',(-0.425,0.0299999999999998,-5.20474889637625E-17));
#8640=CARTESIAN_POINT('Origin',(0.,0.0299999999999998,0.));
#8641=CARTESIAN_POINT('',(-0.425,0.24,-5.20474889637625E-17));
#8642=CARTESIAN_POINT('Origin',(0.,0.0150000000000001,0.));
#8643=CARTESIAN_POINT('',(-0.395,4.85722573273506E-17,-4.83735485663204E-17));
#8644=CARTESIAN_POINT('Origin',(0.,0.,0.));
#8645=CARTESIAN_POINT('',(-0.41,0.0150000000000001,-5.02105187650415E-17));
#8646=CARTESIAN_POINT('Origin',(0.27,0.,0.));
#8647=CARTESIAN_POINT('',(-0.27,0.,-3.30654635769785E-17));
#8648=CARTESIAN_POINT('Origin',(0.,0.,0.));
#8649=CARTESIAN_POINT('Origin',(0.,-0.02,0.));
#8650=CARTESIAN_POINT('',(-0.24505,-0.0498999999999999,3.00099698131059E-17));
#8651=CARTESIAN_POINT('Origin',(0.,-0.0498999999999999,0.));
#8652=CARTESIAN_POINT('',(-0.26,-0.02,-3.18408167778312E-17));
#8653=CARTESIAN_POINT('Origin',(0.,-0.995,0.));
#8654=CARTESIAN_POINT('',(-0.24505,-0.995,-3.00099698131059E-17));
#10576=UNCERTAINTY_MEASURE_WITH_UNIT(LENGTH_MEASURE(0.001),#10651,
'DISTANCE_ACCURACY_VALUE',
'Maximum model space distance between geometric entities at asserted c
onnectivities');
#10611=UNCERTAINTY_MEASURE_WITH_UNIT(LENGTH_MEASURE(0.001),#10651,
'DISTANCE_ACCURACY_VALUE',
'Maximum model space distance between geometric entities at asserted c
onnectivities');
#10615=(
GEOMETRIC_REPRESENTATION_CONTEXT(3)
GLOBAL_UNCERTAINTY_ASSIGNED_CONTEXT((#10576))
GLOBAL_UNIT_ASSIGNED_CONTEXT((#10651,#10653,#10654))
REPRESENTATION_CONTEXT('','3D')
);
#10650=(
GEOMETRIC_REPRESENTATION_CONTEXT(3)
GLOBAL_UNCERTAINTY_ASSIGNED_CONTEXT((#10611))
GLOBAL_UNIT_ASSIGNED_CONTEXT((#10651,#10653,#10654))
REPRESENTATION_CONTEXT('','3D')
);
#10651=(
LENGTH_UNIT()
NAMED_UNIT(*)
SI_UNIT(.CENTI.,.METRE.)
);
#10653=(
NAMED_UNIT(*)
PLANE_ANGLE_UNIT()
SI_UNIT($,.RADIAN.)
);
#10654=(
NAMED_UNIT(*)
SI_UNIT($,.STERADIAN.)
SOLID_ANGLE_UNIT()
);
#10658=SHAPE_DEFINITION_REPRESENTATION(#10696,#10797);
#10696=PRODUCT_DEFINITION_SHAPE('',$,#10836);
#10797=SHAPE_REPRESENTATION('',(#5948),#10615);
#10832=PRODUCT_DEFINITION_CONTEXT('part definition',#10948,'design');
#10836=PRODUCT_DEFINITION('M5x14 Cap Screw','M5x14 Cap Screw',#10874,#10832);
#10874=PRODUCT_DEFINITION_FORMATION('',$,#10953);
#10948=APPLICATION_CONTEXT(
'Core Data for Automotive Mechanical Design Process');
#10949=PRODUCT_CONTEXT('part definition',#10948,'mechanical');
#10953=PRODUCT('M5x14 Cap Screw','M5x14 Cap Screw','M5x14 Cap Screw',(#10949));
#11065=COLOUR_RGB('Black',0.12,0.14,0.17);
#11066=FILL_AREA_STYLE_COLOUR('',#11065);
#11067=FILL_AREA_STYLE('',(#11066));
#11068=SURFACE_STYLE_FILL_AREA(#11067);
#11069=SURFACE_SIDE_STYLE('',(#11068));
#11070=SURFACE_STYLE_USAGE(.BOTH.,#11069);
#11071=PRESENTATION_STYLE_ASSIGNMENT((#11070));
ENDSEC;
END-ISO-10303-21;
